ISO-10303-21;
HEADER;
/* Generated by software containing ST-Developer
 * from STEP Tools, Inc. (www.steptools.com) 
 */

FILE_DESCRIPTION(
/* description */ ('Dual-rail gantry carriage'),
/* implementation_level */ '2;1');

FILE_NAME(
/* name */ 'Captive slot nut.step',
/* time_stamp */ '2026-10-27T10:49:15-07:00',
/* author */ (''),
/* organization */ (''),
/* preprocessor_version */ 'ST-DEVELOPER v20.2',
/* originating_system */ 'Autodesk Translation Framework v15.17.0.0',
/* authorisation */ '');

FILE_SCHEMA (('AUTOMOTIVE_DESIGN { 1 0 10303 214 3 1 1 }'));
ENDSEC;

DATA;
#10=MECHANICAL_DESIGN_GEOMETRIC_PRESENTATION_REPRESENTATION('',(#602),#12804);
#491=ELLIPSE('',#8075,0.299389011154384,0.2117);
#492=ELLIPSE('',#8079,0.299389011154384,0.2117);
#540=SHAPE_REPRESENTATION_RELATIONSHIP('SRR','None',#13018,#571);
#571=ADVANCED_BREP_SHAPE_REPRESENTATION('',(#632),#12788);
#602=STYLED_ITEM('',(#13254),#632);
#632=MANIFOLD_SOLID_BREP('Body1',#7381);
#705=FACE_BOUND('',#1717,.T.);
#931=PLANE('',#8065);
#932=PLANE('',#8066);
#933=PLANE('',#8067);
#934=PLANE('',#8069);
#935=PLANE('',#8070);
#936=PLANE('',#8071);
#937=PLANE('',#8072);
#938=PLANE('',#8073);
#939=PLANE('',#8074);
#940=PLANE('',#8081);
#941=PLANE('',#8082);
#942=PLANE('',#8083);
#943=PLANE('',#8084);
#1262=FACE_OUTER_BOUND('',#1714,.T.);
#1263=FACE_OUTER_BOUND('',#1715,.T.);
#1264=FACE_OUTER_BOUND('',#1716,.T.);
#1265=FACE_OUTER_BOUND('',#1718,.T.);
#1266=FACE_OUTER_BOUND('',#1719,.T.);
#1267=FACE_OUTER_BOUND('',#1720,.T.);
#1268=FACE_OUTER_BOUND('',#1721,.T.);
#1269=FACE_OUTER_BOUND('',#1722,.T.);
#1270=FACE_OUTER_BOUND('',#1723,.T.);
#1271=FACE_OUTER_BOUND('',#1724,.T.);
#1272=FACE_OUTER_BOUND('',#1725,.T.);
#1273=FACE_OUTER_BOUND('',#1726,.T.);
#1274=FACE_OUTER_BOUND('',#1727,.T.);
#1275=FACE_OUTER_BOUND('',#1728,.T.);
#1714=EDGE_LOOP('',(#6081,#6082,#6083,#6084));
#1715=EDGE_LOOP('',(#6085,#6086,#6087,#6088));
#1716=EDGE_LOOP('',(#6089,#6090,#6091,#6092));
#1717=EDGE_LOOP('',(#6093));
#1718=EDGE_LOOP('',(#6094,#6095,#6096,#6097,#6098,#6099,#6100,#6101,#6102,
#6103));
#1719=EDGE_LOOP('',(#6104,#6105,#6106,#6107));
#1720=EDGE_LOOP('',(#6108,#6109,#6110,#6111));
#1721=EDGE_LOOP('',(#6112,#6113,#6114,#6115,#6116,#6117,#6118,#6119,#6120,
#6121));
#1722=EDGE_LOOP('',(#6122,#6123,#6124,#6125));
#1723=EDGE_LOOP('',(#6126,#6127,#6128,#6129,#6130,#6131));
#1724=EDGE_LOOP('',(#6132,#6133,#6134,#6135,#6136,#6137,#6138,#6139));
#1725=EDGE_LOOP('',(#6140,#6141,#6142,#6143,#6144));
#1726=EDGE_LOOP('',(#6145,#6146,#6147,#6148));
#1727=EDGE_LOOP('',(#6149,#6150,#6151,#6152,#6153,#6154));
#1728=EDGE_LOOP('',(#6155,#6156,#6157,#6158));
#2365=LINE('',#11758,#3074);
#2366=LINE('',#11760,#3075);
#2367=LINE('',#11762,#3076);
#2368=LINE('',#11763,#3077);
#2369=LINE('',#11766,#3078);
#2370=LINE('',#11768,#3079);
#2371=LINE('',#11769,#3080);
#2372=LINE('',#11772,#3081);
#2373=LINE('',#11774,#3082);
#2374=LINE('',#11775,#3083);
#2375=LINE('',#11780,#3084);
#2376=LINE('',#11782,#3085);
#2377=LINE('',#11784,#3086);
#2378=LINE('',#11786,#3087);
#2379=LINE('',#11788,#3088);
#2380=LINE('',#11790,#3089);
#2381=LINE('',#11791,#3090);
#2382=LINE('',#11794,#3091);
#2383=LINE('',#11795,#3092);
#2384=LINE('',#11798,#3093);
#2385=LINE('',#11799,#3094);
#2386=LINE('',#11802,#3095);
#2387=LINE('',#11804,#3096);
#2388=LINE('',#11806,#3097);
#2389=LINE('',#11808,#3098);
#2390=LINE('',#11809,#3099);
#2391=LINE('',#11811,#3100);
#2392=LINE('',#11814,#3101);
#2393=LINE('',#11817,#3102);
#2394=LINE('',#11821,#3103);
#2395=LINE('',#11828,#3104);
#2396=LINE('',#11830,#3105);
#2397=LINE('',#11832,#3106);
#3074=VECTOR('',#9554,1.);
#3075=VECTOR('',#9555,1.);
#3076=VECTOR('',#9556,1.);
#3077=VECTOR('',#9557,1.);
#3078=VECTOR('',#9560,1.);
#3079=VECTOR('',#9561,1.);
#3080=VECTOR('',#9562,1.);
#3081=VECTOR('',#9565,1.);
#3082=VECTOR('',#9566,1.);
#3083=VECTOR('',#9567,1.);
#3084=VECTOR('',#9572,1.);
#3085=VECTOR('',#9573,1.);
#3086=VECTOR('',#9574,1.);
#3087=VECTOR('',#9575,1.);
#3088=VECTOR('',#9576,1.);
#3089=VECTOR('',#9577,1.);
#3090=VECTOR('',#9578,1.);
#3091=VECTOR('',#9581,1.);
#3092=VECTOR('',#9582,1.);
#3093=VECTOR('',#9585,1.);
#3094=VECTOR('',#9586,1.);
#3095=VECTOR('',#9589,1.);
#3096=VECTOR('',#9590,1.);
#3097=VECTOR('',#9591,1.);
#3098=VECTOR('',#9592,1.);
#3099=VECTOR('',#9593,1.);
#3100=VECTOR('',#9596,1.);
#3101=VECTOR('',#9599,1.);
#3102=VECTOR('',#9602,1.);
#3103=VECTOR('',#9607,0.21);
#3104=VECTOR('',#9616,1.);
#3105=VECTOR('',#9619,1.);
#3106=VECTOR('',#9622,1.);
#3456=CIRCLE('',#8068,0.2117);
#3457=CIRCLE('',#8077,0.2117);
#3458=CIRCLE('',#8078,0.2117);
#3459=CIRCLE('',#8080,0.2117);
#3892=VERTEX_POINT('',#11756);
#3893=VERTEX_POINT('',#11757);
#3894=VERTEX_POINT('',#11759);
#3895=VERTEX_POINT('',#11761);
#3896=VERTEX_POINT('',#11765);
#3897=VERTEX_POINT('',#11767);
#3898=VERTEX_POINT('',#11771);
#3899=VERTEX_POINT('',#11773);
#3900=VERTEX_POINT('',#11776);
#3901=VERTEX_POINT('',#11779);
#3902=VERTEX_POINT('',#11781);
#3903=VERTEX_POINT('',#11783);
#3904=VERTEX_POINT('',#11785);
#3905=VERTEX_POINT('',#11787);
#3906=VERTEX_POINT('',#11789);
#3907=VERTEX_POINT('',#11793);
#3908=VERTEX_POINT('',#11797);
#3909=VERTEX_POINT('',#11801);
#3910=VERTEX_POINT('',#11803);
#3911=VERTEX_POINT('',#11805);
#3912=VERTEX_POINT('',#11807);
#3913=VERTEX_POINT('',#11813);
#3914=VERTEX_POINT('',#11815);
#3915=VERTEX_POINT('',#11819);
#3916=VERTEX_POINT('',#11822);
#3917=VERTEX_POINT('',#11824);
#4663=EDGE_CURVE('',#3892,#3893,#2365,.T.);
#4664=EDGE_CURVE('',#3894,#3892,#2366,.T.);
#4665=EDGE_CURVE('',#3895,#3894,#2367,.T.);
#4666=EDGE_CURVE('',#3893,#3895,#2368,.T.);
#4667=EDGE_CURVE('',#3894,#3896,#2369,.T.);
#4668=EDGE_CURVE('',#3897,#3896,#2370,.T.);
#4669=EDGE_CURVE('',#3895,#3897,#2371,.T.);
#4670=EDGE_CURVE('',#3896,#3898,#2372,.T.);
#4671=EDGE_CURVE('',#3898,#3899,#2373,.T.);
#4672=EDGE_CURVE('',#3899,#3897,#2374,.T.);
#4673=EDGE_CURVE('',#3900,#3900,#3456,.T.);
#4674=EDGE_CURVE('',#3901,#3892,#2375,.T.);
#4675=EDGE_CURVE('',#3902,#3901,#2376,.T.);
#4676=EDGE_CURVE('',#3902,#3903,#2377,.T.);
#4677=EDGE_CURVE('',#3904,#3903,#2378,.T.);
#4678=EDGE_CURVE('',#3904,#3905,#2379,.T.);
#4679=EDGE_CURVE('',#3905,#3906,#2380,.T.);
#4680=EDGE_CURVE('',#3906,#3898,#2381,.T.);
#4681=EDGE_CURVE('',#3906,#3907,#2382,.T.);
#4682=EDGE_CURVE('',#3907,#3899,#2383,.T.);
#4683=EDGE_CURVE('',#3908,#3905,#2384,.T.);
#4684=EDGE_CURVE('',#3907,#3908,#2385,.T.);
#4685=EDGE_CURVE('',#3909,#3908,#2386,.T.);
#4686=EDGE_CURVE('',#3910,#3909,#2387,.T.);
#4687=EDGE_CURVE('',#3910,#3911,#2388,.T.);
#4688=EDGE_CURVE('',#3912,#3911,#2389,.T.);
#4689=EDGE_CURVE('',#3912,#3893,#2390,.T.);
#4690=EDGE_CURVE('',#3909,#3904,#2391,.T.);
#4691=EDGE_CURVE('',#3903,#3913,#2392,.T.);
#4692=EDGE_CURVE('',#3913,#3914,#491,.T.);
#4693=EDGE_CURVE('',#3914,#3910,#2393,.T.);
#4694=EDGE_CURVE('',#3915,#3913,#3457,.F.);
#4695=EDGE_CURVE('',#3915,#3900,#2394,.T.);
#4696=EDGE_CURVE('',#3916,#3915,#3458,.F.);
#4697=EDGE_CURVE('',#3917,#3916,#492,.T.);
#4698=EDGE_CURVE('',#3914,#3917,#3459,.F.);
#4699=EDGE_CURVE('',#3916,#3902,#2395,.T.);
#4700=EDGE_CURVE('',#3911,#3917,#2396,.T.);
#4701=EDGE_CURVE('',#3901,#3912,#2397,.T.);
#6081=ORIENTED_EDGE('',*,*,#4663,.F.);
#6082=ORIENTED_EDGE('',*,*,#4664,.F.);
#6083=ORIENTED_EDGE('',*,*,#4665,.F.);
#6084=ORIENTED_EDGE('',*,*,#4666,.F.);
#6085=ORIENTED_EDGE('',*,*,#4665,.T.);
#6086=ORIENTED_EDGE('',*,*,#4667,.T.);
#6087=ORIENTED_EDGE('',*,*,#4668,.F.);
#6088=ORIENTED_EDGE('',*,*,#4669,.F.);
#6089=ORIENTED_EDGE('',*,*,#4670,.T.);
#6090=ORIENTED_EDGE('',*,*,#4671,.T.);
#6091=ORIENTED_EDGE('',*,*,#4672,.T.);
#6092=ORIENTED_EDGE('',*,*,#4668,.T.);
#6093=ORIENTED_EDGE('',*,*,#4673,.T.);
#6094=ORIENTED_EDGE('',*,*,#4670,.F.);
#6095=ORIENTED_EDGE('',*,*,#4667,.F.);
#6096=ORIENTED_EDGE('',*,*,#4664,.T.);
#6097=ORIENTED_EDGE('',*,*,#4674,.F.);
#6098=ORIENTED_EDGE('',*,*,#4675,.F.);
#6099=ORIENTED_EDGE('',*,*,#4676,.T.);
#6100=ORIENTED_EDGE('',*,*,#4677,.F.);
#6101=ORIENTED_EDGE('',*,*,#4678,.T.);
#6102=ORIENTED_EDGE('',*,*,#4679,.T.);
#6103=ORIENTED_EDGE('',*,*,#4680,.T.);
#6104=ORIENTED_EDGE('',*,*,#4681,.T.);
#6105=ORIENTED_EDGE('',*,*,#4682,.T.);
#6106=ORIENTED_EDGE('',*,*,#4671,.F.);
#6107=ORIENTED_EDGE('',*,*,#4680,.F.);
#6108=ORIENTED_EDGE('',*,*,#4683,.F.);
#6109=ORIENTED_EDGE('',*,*,#4684,.F.);
#6110=ORIENTED_EDGE('',*,*,#4681,.F.);
#6111=ORIENTED_EDGE('',*,*,#4679,.F.);
#6112=ORIENTED_EDGE('',*,*,#4672,.F.);
#6113=ORIENTED_EDGE('',*,*,#4682,.F.);
#6114=ORIENTED_EDGE('',*,*,#4684,.T.);
#6115=ORIENTED_EDGE('',*,*,#4685,.F.);
#6116=ORIENTED_EDGE('',*,*,#4686,.F.);
#6117=ORIENTED_EDGE('',*,*,#4687,.T.);
#6118=ORIENTED_EDGE('',*,*,#4688,.F.);
#6119=ORIENTED_EDGE('',*,*,#4689,.T.);
#6120=ORIENTED_EDGE('',*,*,#4666,.T.);
#6121=ORIENTED_EDGE('',*,*,#4669,.T.);
#6122=ORIENTED_EDGE('',*,*,#4683,.T.);
#6123=ORIENTED_EDGE('',*,*,#4678,.F.);
#6124=ORIENTED_EDGE('',*,*,#4690,.F.);
#6125=ORIENTED_EDGE('',*,*,#4685,.T.);
#6126=ORIENTED_EDGE('',*,*,#4686,.T.);
#6127=ORIENTED_EDGE('',*,*,#4690,.T.);
#6128=ORIENTED_EDGE('',*,*,#4677,.T.);
#6129=ORIENTED_EDGE('',*,*,#4691,.T.);
#6130=ORIENTED_EDGE('',*,*,#4692,.T.);
#6131=ORIENTED_EDGE('',*,*,#4693,.T.);
#6132=ORIENTED_EDGE('',*,*,#4692,.F.);
#6133=ORIENTED_EDGE('',*,*,#4694,.F.);
#6134=ORIENTED_EDGE('',*,*,#4695,.T.);
#6135=ORIENTED_EDGE('',*,*,#4673,.F.);
#6136=ORIENTED_EDGE('',*,*,#4695,.F.);
#6137=ORIENTED_EDGE('',*,*,#4696,.F.);
#6138=ORIENTED_EDGE('',*,*,#4697,.F.);
#6139=ORIENTED_EDGE('',*,*,#4698,.F.);
#6140=ORIENTED_EDGE('',*,*,#4691,.F.);
#6141=ORIENTED_EDGE('',*,*,#4676,.F.);
#6142=ORIENTED_EDGE('',*,*,#4699,.F.);
#6143=ORIENTED_EDGE('',*,*,#4696,.T.);
#6144=ORIENTED_EDGE('',*,*,#4694,.T.);
#6145=ORIENTED_EDGE('',*,*,#4693,.F.);
#6146=ORIENTED_EDGE('',*,*,#4698,.T.);
#6147=ORIENTED_EDGE('',*,*,#4700,.F.);
#6148=ORIENTED_EDGE('',*,*,#4687,.F.);
#6149=ORIENTED_EDGE('',*,*,#4675,.T.);
#6150=ORIENTED_EDGE('',*,*,#4701,.T.);
#6151=ORIENTED_EDGE('',*,*,#4688,.T.);
#6152=ORIENTED_EDGE('',*,*,#4700,.T.);
#6153=ORIENTED_EDGE('',*,*,#4697,.T.);
#6154=ORIENTED_EDGE('',*,*,#4699,.T.);
#6155=ORIENTED_EDGE('',*,*,#4663,.T.);
#6156=ORIENTED_EDGE('',*,*,#4689,.F.);
#6157=ORIENTED_EDGE('',*,*,#4701,.F.);
#6158=ORIENTED_EDGE('',*,*,#4674,.T.);
#6932=CYLINDRICAL_SURFACE('',#8076,0.2117);
#7188=ADVANCED_FACE('',(#1262),#931,.F.);
#7189=ADVANCED_FACE('',(#1263),#932,.T.);
#7190=ADVANCED_FACE('',(#1264,#705),#933,.T.);
#7191=ADVANCED_FACE('',(#1265),#934,.T.);
#7192=ADVANCED_FACE('',(#1266),#935,.T.);
#7193=ADVANCED_FACE('',(#1267),#936,.F.);
#7194=ADVANCED_FACE('',(#1268),#937,.T.);
#7195=ADVANCED_FACE('',(#1269),#938,.T.);
#7196=ADVANCED_FACE('',(#1270),#939,.T.);
#7197=ADVANCED_FACE('',(#1271),#6932,.F.);
#7198=ADVANCED_FACE('',(#1272),#940,.F.);
#7199=ADVANCED_FACE('',(#1273),#941,.F.);
#7200=ADVANCED_FACE('',(#1274),#942,.T.);
#7201=ADVANCED_FACE('',(#1275),#943,.T.);
#7381=CLOSED_SHELL('',(#7188,#7189,#7190,#7191,#7192,#7193,#7194,#7195,
#7196,#7197,#7198,#7199,#7200,#7201));
#8064=AXIS2_PLACEMENT_3D('',#11754,#9550,#9551);
#8065=AXIS2_PLACEMENT_3D('',#11755,#9552,#9553);
#8066=AXIS2_PLACEMENT_3D('',#11764,#9558,#9559);
#8067=AXIS2_PLACEMENT_3D('',#11770,#9563,#9564);
#8068=AXIS2_PLACEMENT_3D('',#11777,#9568,#9569);
#8069=AXIS2_PLACEMENT_3D('',#11778,#9570,#9571);
#8070=AXIS2_PLACEMENT_3D('',#11792,#9579,#9580);
#8071=AXIS2_PLACEMENT_3D('',#11796,#9583,#9584);
#8072=AXIS2_PLACEMENT_3D('',#11800,#9587,#9588);
#8073=AXIS2_PLACEMENT_3D('',#11810,#9594,#9595);
#8074=AXIS2_PLACEMENT_3D('',#11812,#9597,#9598);
#8075=AXIS2_PLACEMENT_3D('',#11816,#9600,#9601);
#8076=AXIS2_PLACEMENT_3D('',#11818,#9603,#9604);
#8077=AXIS2_PLACEMENT_3D('',#11820,#9605,#9606);
#8078=AXIS2_PLACEMENT_3D('',#11823,#9608,#9609);
#8079=AXIS2_PLACEMENT_3D('',#11825,#9610,#9611);
#8080=AXIS2_PLACEMENT_3D('',#11826,#9612,#9613);
#8081=AXIS2_PLACEMENT_3D('',#11827,#9614,#9615);
#8082=AXIS2_PLACEMENT_3D('',#11829,#9617,#9618);
#8083=AXIS2_PLACEMENT_3D('',#11831,#9620,#9621);
#8084=AXIS2_PLACEMENT_3D('',#11833,#9623,#9624);
#9550=DIRECTION('axis',(0.,0.,1.));
#9551=DIRECTION('refdir',(1.,0.,0.));
#9552=DIRECTION('center_axis',(0.,0.,1.));
#9553=DIRECTION('ref_axis',(1.,0.,0.));
#9554=DIRECTION('',(1.,0.,0.));
#9555=DIRECTION('',(0.,-1.,0.));
#9556=DIRECTION('',(-1.,0.,0.));
#9557=DIRECTION('',(0.,1.,0.));
#9558=DIRECTION('center_axis',(0.,1.,0.));
#9559=DIRECTION('ref_axis',(-1.,0.,0.));
#9560=DIRECTION('',(0.,0.,1.));
#9561=DIRECTION('',(-1.,0.,0.));
#9562=DIRECTION('',(0.,0.,1.));
#9563=DIRECTION('center_axis',(0.,0.,1.));
#9564=DIRECTION('ref_axis',(1.,0.,0.));
#9565=DIRECTION('',(0.,-1.,0.));
#9566=DIRECTION('',(1.,0.,0.));
#9567=DIRECTION('',(0.,1.,0.));
#9568=DIRECTION('center_axis',(0.,0.,-1.));
#9569=DIRECTION('ref_axis',(1.,0.,0.));
#9570=DIRECTION('center_axis',(-1.,0.,0.));
#9571=DIRECTION('ref_axis',(0.,-1.,0.));
#9572=DIRECTION('',(0.,0.,1.));
#9573=DIRECTION('',(0.,0.707106781186548,0.707106781186548));
#9574=DIRECTION('',(0.,-1.,0.));
#9575=DIRECTION('',(0.,0.707106781186548,-0.707106781186548));
#9576=DIRECTION('',(0.,0.,1.));
#9577=DIRECTION('',(0.,-1.,0.));
#9578=DIRECTION('',(0.,0.,1.));
#9579=DIRECTION('center_axis',(0.,-1.,0.));
#9580=DIRECTION('ref_axis',(1.,0.,0.));
#9581=DIRECTION('',(1.,0.,0.));
#9582=DIRECTION('',(0.,0.,1.));
#9583=DIRECTION('center_axis',(0.,0.,1.));
#9584=DIRECTION('ref_axis',(1.,0.,0.));
#9585=DIRECTION('',(-1.,0.,0.));
#9586=DIRECTION('',(0.,1.,0.));
#9587=DIRECTION('center_axis',(1.,0.,0.));
#9588=DIRECTION('ref_axis',(0.,1.,0.));
#9589=DIRECTION('',(0.,0.,1.));
#9590=DIRECTION('',(0.,-0.707106781186548,0.707106781186548));
#9591=DIRECTION('',(0.,1.,0.));
#9592=DIRECTION('',(0.,-0.707106781186548,-0.707106781186548));
#9593=DIRECTION('',(0.,0.,1.));
#9594=DIRECTION('center_axis',(0.,-1.,0.));
#9595=DIRECTION('ref_axis',(1.,0.,0.));
#9596=DIRECTION('',(-1.,0.,0.));
#9597=DIRECTION('center_axis',(0.,-0.707106781186548,-0.707106781186548));
#9598=DIRECTION('ref_axis',(-1.,0.,0.));
#9599=DIRECTION('',(1.,0.,0.));
#9600=DIRECTION('center_axis',(0.,0.707106781186548,0.707106781186548));
#9601=DIRECTION('ref_axis',(0.,0.707106781186547,-0.707106781186547));
#9602=DIRECTION('',(1.,0.,0.));
#9603=DIRECTION('center_axis',(0.,0.,1.));
#9604=DIRECTION('ref_axis',(1.,0.,0.));
#9605=DIRECTION('center_axis',(0.,0.,-1.));
#9606=DIRECTION('ref_axis',(1.,0.,0.));
#9607=DIRECTION('',(0.,0.,1.));
#9608=DIRECTION('center_axis',(0.,0.,-1.));
#9609=DIRECTION('ref_axis',(1.,0.,0.));
#9610=DIRECTION('center_axis',(0.,-0.707106781186548,0.707106781186548));
#9611=DIRECTION('ref_axis',(0.,0.707106781186547,0.707106781186547));
#9612=DIRECTION('center_axis',(0.,0.,-1.));
#9613=DIRECTION('ref_axis',(1.,0.,0.));
#9614=DIRECTION('center_axis',(0.,0.,1.));
#9615=DIRECTION('ref_axis',(1.,0.,0.));
#9616=DIRECTION('',(-1.,0.,0.));
#9617=DIRECTION('center_axis',(0.,0.,1.));
#9618=DIRECTION('ref_axis',(1.,0.,0.));
#9619=DIRECTION('',(-1.,0.,0.));
#9620=DIRECTION('center_axis',(0.,0.707106781186548,-0.707106781186548));
#9621=DIRECTION('ref_axis',(-1.,0.,0.));
#9622=DIRECTION('',(1.,0.,0.));
#9623=DIRECTION('center_axis',(0.,1.,0.));
#9624=DIRECTION('ref_axis',(-1.,0.,0.));
#11754=CARTESIAN_POINT('',(0.,0.,0.));
#11755=CARTESIAN_POINT('Origin',(0.,0.395,0.25));
#11756=CARTESIAN_POINT('',(-0.5,0.3,0.25));
#11757=CARTESIAN_POINT('',(0.5,0.3,0.25));
#11758=CARTESIAN_POINT('',(0.25,0.3,0.25));
#11759=CARTESIAN_POINT('',(-0.5,0.5,0.25));
#11760=CARTESIAN_POINT('',(-0.5,0.5,0.25));
#11761=CARTESIAN_POINT('',(0.5,0.5,0.25));
#11762=CARTESIAN_POINT('',(0.5,0.5,0.25));
#11763=CARTESIAN_POINT('',(0.5,0.29,0.25));
#11764=CARTESIAN_POINT('Origin',(0.5,0.5,0.25));
#11765=CARTESIAN_POINT('',(-0.5,0.5,0.4));
#11766=CARTESIAN_POINT('',(-0.5,0.5,0.25));
#11767=CARTESIAN_POINT('',(0.5,0.5,0.4));
#11768=CARTESIAN_POINT('',(0.5,0.5,0.4));
#11769=CARTESIAN_POINT('',(0.5,0.5,0.25));
#11770=CARTESIAN_POINT('Origin',(0.,0.,0.4));
#11771=CARTESIAN_POINT('',(-0.5,-0.5,0.4));
#11772=CARTESIAN_POINT('',(-0.5,0.5,0.4));
#11773=CARTESIAN_POINT('',(0.5,-0.5,0.4));
#11774=CARTESIAN_POINT('',(-0.5,-0.5,0.4));
#11775=CARTESIAN_POINT('',(0.5,-0.3,0.4));
#11776=CARTESIAN_POINT('',(-0.2117,2.59257727379495E-17,0.4));
#11777=CARTESIAN_POINT('Origin',(0.,0.,0.4));
#11778=CARTESIAN_POINT('Origin',(-0.5,0.3,0.));
#11779=CARTESIAN_POINT('',(-0.5,0.3,0.15));
#11780=CARTESIAN_POINT('',(-0.5,0.3,0.));
#11781=CARTESIAN_POINT('',(-0.5,0.15,0.));
#11782=CARTESIAN_POINT('',(-0.5,0.225,0.075));
#11783=CARTESIAN_POINT('',(-0.5,-0.15,0.));
#11784=CARTESIAN_POINT('',(-0.5,0.3,0.));
#11785=CARTESIAN_POINT('',(-0.5,-0.3,0.15));
#11786=CARTESIAN_POINT('',(-0.5,-0.075,-0.075));
#11787=CARTESIAN_POINT('',(-0.5,-0.3,0.25));
#11788=CARTESIAN_POINT('',(-0.5,-0.3,0.));
#11789=CARTESIAN_POINT('',(-0.5,-0.5,0.25));
#11790=CARTESIAN_POINT('',(-0.5,-0.29,0.25));
#11791=CARTESIAN_POINT('',(-0.5,-0.5,0.25));
#11792=CARTESIAN_POINT('Origin',(-0.5,-0.5,0.25));
#11793=CARTESIAN_POINT('',(0.5,-0.5,0.25));
#11794=CARTESIAN_POINT('',(-0.5,-0.5,0.25));
#11795=CARTESIAN_POINT('',(0.5,-0.5,0.25));
#11796=CARTESIAN_POINT('Origin',(0.,-0.395,0.25));
#11797=CARTESIAN_POINT('',(0.5,-0.3,0.25));
#11798=CARTESIAN_POINT('',(-0.25,-0.3,0.25));
#11799=CARTESIAN_POINT('',(0.5,-0.5,0.25));
#11800=CARTESIAN_POINT('Origin',(0.5,-0.3,0.));
#11801=CARTESIAN_POINT('',(0.5,-0.3,0.15));
#11802=CARTESIAN_POINT('',(0.5,-0.3,0.));
#11803=CARTESIAN_POINT('',(0.5,-0.15,0.));
#11804=CARTESIAN_POINT('',(0.5,-0.225,0.075));
#11805=CARTESIAN_POINT('',(0.5,0.15,0.));
#11806=CARTESIAN_POINT('',(0.5,-0.3,0.));
#11807=CARTESIAN_POINT('',(0.5,0.3,0.15));
#11808=CARTESIAN_POINT('',(0.5,0.075,-0.075));
#11809=CARTESIAN_POINT('',(0.5,0.3,0.));
#11810=CARTESIAN_POINT('Origin',(-0.5,-0.3,0.));
#11811=CARTESIAN_POINT('',(-0.25,-0.3,0.15));
#11812=CARTESIAN_POINT('Origin',(-0.25,-0.225,0.075));
#11813=CARTESIAN_POINT('',(-0.149388386429468,-0.15,0.));
#11814=CARTESIAN_POINT('',(-0.25,-0.15,0.));
#11815=CARTESIAN_POINT('',(0.149388386429468,-0.15,0.));
#11816=CARTESIAN_POINT('Origin',(0.,0.,-0.15));
#11817=CARTESIAN_POINT('',(-0.25,-0.15,0.));
#11818=CARTESIAN_POINT('Origin',(0.,0.,-0.1));
#11819=CARTESIAN_POINT('',(-0.2117,-2.59257727379495E-17,0.));
#11820=CARTESIAN_POINT('Origin',(0.,0.,0.));
#11821=CARTESIAN_POINT('',(-0.2117,-2.59257727379495E-17,-0.1));
#11822=CARTESIAN_POINT('',(-0.149388386429468,0.15,0.));
#11823=CARTESIAN_POINT('Origin',(0.,0.,0.));
#11824=CARTESIAN_POINT('',(0.149388386429468,0.15,0.));
#11825=CARTESIAN_POINT('Origin',(0.,0.,-0.15));
#11826=CARTESIAN_POINT('Origin',(0.,0.,0.));
#11827=CARTESIAN_POINT('Origin',(0.,0.,0.));
#11828=CARTESIAN_POINT('',(0.25,0.15,0.));
#11829=CARTESIAN_POINT('Origin',(0.,0.,0.));
#11830=CARTESIAN_POINT('',(0.25,0.15,0.));
#11831=CARTESIAN_POINT('Origin',(0.25,0.225,0.075));
#11832=CARTESIAN_POINT('',(0.25,0.3,0.15));
#11833=CARTESIAN_POINT('Origin',(0.5,0.3,0.));
#12752=UNCERTAINTY_MEASURE_WITH_UNIT(LENGTH_MEASURE(0.001),#12805,
'DISTANCE_ACCURACY_VALUE',
'Maximum model space distance between geometric entities at asserted c
onnectivities');
#12768=UNCERTAINTY_MEASURE_WITH_UNIT(LENGTH_MEASURE(0.001),#12805,
'DISTANCE_ACCURACY_VALUE',
'Maximum model space distance between geometric entities at asserted c
onnectivities');
#12788=(
GEOMETRIC_REPRESENTATION_CONTEXT(3)
GLOBAL_UNCERTAINTY_ASSIGNED_CONTEXT((#12752))
GLOBAL_UNIT_ASSIGNED_CONTEXT((#12805,#12807,#12808))
REPRESENTATION_CONTEXT('','3D')
);
#12804=(
GEOMETRIC_REPRESENTATION_CONTEXT(3)
GLOBAL_UNCERTAINTY_ASSIGNED_CONTEXT((#12768))
GLOBAL_UNIT_ASSIGNED_CONTEXT((#12805,#12807,#12808))
REPRESENTATION_CONTEXT('','3D')
);
#12805=(
LENGTH_UNIT()
NAMED_UNIT(*)
SI_UNIT(.CENTI.,.METRE.)
);
#12807=(
NAMED_UNIT(*)
PLANE_ANGLE_UNIT()
SI_UNIT($,.RADIAN.)
);
#12808=(
NAMED_UNIT(*)
SI_UNIT($,.STERADIAN.)
SOLID_ANGLE_UNIT()
);
#12828=SHAPE_DEFINITION_REPRESENTATION(#12863,#13018);
#12863=PRODUCT_DEFINITION_SHAPE('',$,#13054);
#13018=SHAPE_REPRESENTATION('',(#8064),#12788);
#13034=PRODUCT_DEFINITION_CONTEXT('part definition',#13141,'design');
#13054=PRODUCT_DEFINITION('Captive slot nut','Captive slot nut',#13089,
#13034);
#13089=PRODUCT_DEFINITION_FORMATION('',$,#13162);
#13141=APPLICATION_CONTEXT(
'Core Data for Automotive Mechanical Design Process');
#13142=PRODUCT_CONTEXT('part definition',#13141,'mechanical');
#13162=PRODUCT('Captive slot nut','Captive slot nut','Captive slot nut',
(#13142));
#13248=COLOUR_RGB('Black',0.12,0.14,0.17);
#13249=FILL_AREA_STYLE_COLOUR('',#13248);
#13250=FILL_AREA_STYLE('',(#13249));
#13251=SURFACE_STYLE_FILL_AREA(#13250);
#13252=SURFACE_SIDE_STYLE('',(#13251));
#13253=SURFACE_STYLE_USAGE(.BOTH.,#13252);
#13254=PRESENTATION_STYLE_ASSIGNMENT((#13253));
ENDSEC;
END-ISO-10303-21;
